ISO-10303-21;
HEADER;
/* Generated by software containing ST-Developer
 * from STEP Tools, Inc. (www.steptools.com) 
 */

FILE_DESCRIPTION(
/* description */ (''),
/* implementation_level */ '2;1');

FILE_NAME(
/* name */ 'Spring_04.step',
/* time_stamp */ '2026-10-23T17:00:58+06:00',
/* author */ (''),
/* organization */ (''),
/* preprocessor_version */ 'ST-DEVELOPER v20.2',
/* originating_system */ 'Autodesk Translation Framework v15.15.0.0',
/* authorisation */ '');

FILE_SCHEMA (('AUTOMOTIVE_DESIGN { 1 0 10303 214 3 1 1 }'));
ENDSEC;

DATA;
#10=MECHANICAL_DESIGN_GEOMETRIC_PRESENTATION_REPRESENTATION('',(#113),#11385);
#70=B_SPLINE_SURFACE_WITH_KNOTS('',3,3,((#9768,#9769,#9770,#9771,#9772,
#9773,#9774,#9775,#9776,#9777,#9778,#9779,#9780,#9781,#9782,#9783,#9784,
#9785,#9786,#9787,#9788,#9789,#9790,#9791,#9792,#9793,#9794,#9795,#9796,
#9797,#9798,#9799,#9800,#9801,#9802,#9803,#9804),(#9805,#9806,#9807,#9808,
#9809,#9810,#9811,#9812,#9813,#9814,#9815,#9816,#9817,#9818,#9819,#9820,
#9821,#9822,#9823,#9824,#9825,#9826,#9827,#9828,#9829,#9830,#9831,#9832,
#9833,#9834,#9835,#9836,#9837,#9838,#9839,#9840,#9841),(#9842,#9843,#9844,
#9845,#9846,#9847,#9848,#9849,#9850,#9851,#9852,#9853,#9854,#9855,#9856,
#9857,#9858,#9859,#9860,#9861,#9862,#9863,#9864,#9865,#9866,#9867,#9868,
#9869,#9870,#9871,#9872,#9873,#9874,#9875,#9876,#9877,#9878),(#9879,#9880,
#9881,#9882,#9883,#9884,#9885,#9886,#9887,#9888,#9889,#9890,#9891,#9892,
#9893,#9894,#9895,#9896,#9897,#9898,#9899,#9900,#9901,#9902,#9903,#9904,
#9905,#9906,#9907,#9908,#9909,#9910,#9911,#9912,#9913,#9914,#9915),(#9916,
#9917,#9918,#9919,#9920,#9921,#9922,#9923,#9924,#9925,#9926,#9927,#9928,
#9929,#9930,#9931,#9932,#9933,#9934,#9935,#9936,#9937,#9938,#9939,#9940,
#9941,#9942,#9943,#9944,#9945,#9946,#9947,#9948,#9949,#9950,#9951,#9952),
(#9953,#9954,#9955,#9956,#9957,#9958,#9959,#9960,#9961,#9962,#9963,#9964,
#9965,#9966,#9967,#9968,#9969,#9970,#9971,#9972,#9973,#9974,#9975,#9976,
#9977,#9978,#9979,#9980,#9981,#9982,#9983,#9984,#9985,#9986,#9987,#9988,
#9989),(#9990,#9991,#9992,#9993,#9994,#9995,#9996,#9997,#9998,#9999,#10000,
#10001,#10002,#10003,#10004,#10005,#10006,#10007,#10008,#10009,#10010,#10011,
#10012,#10013,#10014,#10015,#10016,#10017,#10018,#10019,#10020,#10021,#10022,
#10023,#10024,#10025,#10026),(#10027,#10028,#10029,#10030,#10031,#10032,
#10033,#10034,#10035,#10036,#10037,#10038,#10039,#10040,#10041,#10042,#10043,
#10044,#10045,#10046,#10047,#10048,#10049,#10050,#10051,#10052,#10053,#10054,
#10055,#10056,#10057,#10058,#10059,#10060,#10061,#10062,#10063),(#10064,
#10065,#10066,#10067,#10068,#10069,#10070,#10071,#10072,#10073,#10074,#10075,
#10076,#10077,#10078,#10079,#10080,#10081,#10082,#10083,#10084,#10085,#10086,
#10087,#10088,#10089,#10090,#10091,#10092,#10093,#10094,#10095,#10096,#10097,
#10098,#10099,#10100),(#10101,#10102,#10103,#10104,#10105,#10106,#10107,
#10108,#10109,#10110,#10111,#10112,#10113,#10114,#10115,#10116,#10117,#10118,
#10119,#10120,#10121,#10122,#10123,#10124,#10125,#10126,#10127,#10128,#10129,
#10130,#10131,#10132,#10133,#10134,#10135,#10136,#10137),(#10138,#10139,
#10140,#10141,#10142,#10143,#10144,#10145,#10146,#10147,#10148,#10149,#10150,
#10151,#10152,#10153,#10154,#10155,#10156,#10157,#10158,#10159,#10160,#10161,
#10162,#10163,#10164,#10165,#10166,#10167,#10168,#10169,#10170,#10171,#10172,
#10173,#10174),(#10175,#10176,#10177,#10178,#10179,#10180,#10181,#10182,
#10183,#10184,#10185,#10186,#10187,#10188,#10189,#10190,#10191,#10192,#10193,
#10194,#10195,#10196,#10197,#10198,#10199,#10200,#10201,#10202,#10203,#10204,
#10205,#10206,#10207,#10208,#10209,#10210,#10211)),.UNSPECIFIED.,.T.,.F.,
 .F.,(4,1,1,1,1,1,1,1,1,4),(4,1,1,1,1,1,1,1,1,1,1,1,1,1,1,1,1,1,1,1,1,1,
1,1,1,1,1,1,1,1,1,1,1,1,4),(-3.14159265358979,-2.46839422782055,-2.24399475256414,
-1.79519580205131,-1.12199737628207,-0.448798950512828,0.448798950512828,
1.34639685153848,2.24399475256414,3.14159265358979),(0.,0.490873852123405,
0.98174770424681,1.96349540849362,2.94524311274043,3.92699081698724,4.90873852123405,
5.89048622548086,6.87223392972767,7.85398163397448,8.83572933822129,9.8174770424681,
10.7992247467149,11.7809724509617,12.7627201552085,13.7444678594553,14.7262155637022,
15.707963267949,16.6897109721958,17.6714586764426,18.6532063806894,19.6349540849362,
20.616701789183,21.5984494934298,22.5801971976766,23.5619449019234,24.5436926061703,
25.5254403104171,26.5071880146639,27.4889357189107,28.4706834231575,29.4524311274043,
30.4341788316511,30.9250526837745,31.4159265358979),.UNSPECIFIED.);
#76=TOROIDAL_SURFACE('',#6036,1.,0.25);
#87=SHAPE_REPRESENTATION_RELATIONSHIP('SRR','None',#11439,#100);
#100=ADVANCED_BREP_SHAPE_REPRESENTATION('',(#126),#11379);
#113=STYLED_ITEM('',(#11567),#126);
#126=MANIFOLD_SOLID_BREP('Spring_04',#5349);
#168=FACE_BOUND('',#1261,.T.);
#177=B_SPLINE_CURVE_WITH_KNOTS('',3,(#9724,#9725,#9726,#9727,#9728,#9729,
#9730,#9731,#9732,#9733,#9734,#9735,#9736,#9737,#9738,#9739,#9740,#9741,
#9742,#9743,#9744,#9745,#9746,#9747,#9748,#9749,#9750,#9751,#9752,#9753,
#9754,#9755,#9756,#9757,#9758,#9759,#9760,#9761,#9762,#9763,#9764,#9765,
#9766,#9767),.UNSPECIFIED.,.F.,.F.,(4,2,2,2,2,2,2,2,2,2,2,2,2,2,2,2,2,2,
2,2,2,4),(-0.181685657499379,-0.180553745361431,-0.170622434730818,-0.170447684206912,
-0.167737370927117,-0.166612489538818,-0.16575101153334,-0.16478662015514,
-0.16342132279605,-0.160072321773434,-0.151029759575816,-0.145020173168477,
-0.126301129887337,-0.111561605759352,-0.101015311157688,-0.0928919097586381,
-0.0856896815461206,-0.0776947291824182,-0.0660486167614411,-0.0443043011100664,
0.,0.000811103137473634),.UNSPECIFIED.);
#178=B_SPLINE_CURVE_WITH_KNOTS('',3,(#10213,#10214,#10215,#10216,#10217,
#10218,#10219,#10220,#10221,#10222,#10223,#10224,#10225,#10226,#10227,#10228,
#10229,#10230,#10231,#10232,#10233,#10234,#10235,#10236,#10237,#10238,#10239,
#10240,#10241,#10242,#10243,#10244,#10245,#10246,#10247,#10248,#10249),
 .UNSPECIFIED.,.F.,.F.,(4,1,1,1,1,1,1,1,1,1,1,1,1,1,1,1,1,1,1,1,1,1,1,1,
1,1,1,1,1,1,1,1,1,1,4),(0.,0.490873852123405,0.98174770424681,1.96349540849362,
2.94524311274043,3.92699081698724,4.90873852123405,5.89048622548086,6.87223392972767,
7.85398163397448,8.83572933822129,9.8174770424681,10.7992247467149,11.7809724509617,
12.7627201552085,13.7444678594553,14.7262155637022,15.707963267949,16.6897109721958,
17.6714586764426,18.6532063806894,19.6349540849362,20.616701789183,21.5984494934298,
22.5801971976766,23.5619449019234,24.5436926061703,25.5254403104171,26.5071880146639,
27.4889357189107,28.4706834231575,29.4524311274043,30.4341788316511,30.9250526837745,
31.4159265358979),.UNSPECIFIED.);
#508=CIRCLE('',#6037,0.25);
#509=CIRCLE('',#6038,0.75);
#510=CIRCLE('',#6039,0.25);
#511=CIRCLE('',#6040,0.25);
#898=FACE_OUTER_BOUND('',#1260,.T.);
#899=FACE_OUTER_BOUND('',#1262,.T.);
#900=FACE_OUTER_BOUND('',#1263,.T.);
#1260=EDGE_LOOP('',(#4748,#4749,#4750,#4751));
#1261=EDGE_LOOP('',(#4752,#4753));
#1262=EDGE_LOOP('',(#4754,#4755,#4756,#4757,#4758));
#1263=EDGE_LOOP('',(#4759));
#2626=VERTEX_POINT('',#9718);
#2627=VERTEX_POINT('',#9721);
#2628=VERTEX_POINT('',#9722);
#2629=VERTEX_POINT('',#10212);
#3339=EDGE_CURVE('',#2626,#2626,#508,.T.);
#3340=EDGE_CURVE('',#2626,#2626,#509,.T.);
#3341=EDGE_CURVE('',#2627,#2628,#510,.T.);
#3342=EDGE_CURVE('',#2627,#2628,#177,.T.);
#3343=EDGE_CURVE('',#2628,#2629,#178,.T.);
#3344=EDGE_CURVE('',#2629,#2629,#511,.T.);
#4748=ORIENTED_EDGE('',*,*,#3339,.T.);
#4749=ORIENTED_EDGE('',*,*,#3340,.T.);
#4750=ORIENTED_EDGE('',*,*,#3339,.F.);
#4751=ORIENTED_EDGE('',*,*,#3340,.F.);
#4752=ORIENTED_EDGE('',*,*,#3341,.F.);
#4753=ORIENTED_EDGE('',*,*,#3342,.T.);
#4754=ORIENTED_EDGE('',*,*,#3342,.F.);
#4755=ORIENTED_EDGE('',*,*,#3341,.T.);
#4756=ORIENTED_EDGE('',*,*,#3343,.T.);
#4757=ORIENTED_EDGE('',*,*,#3344,.T.);
#4758=ORIENTED_EDGE('',*,*,#3343,.F.);
#4759=ORIENTED_EDGE('',*,*,#3344,.F.);
#5000=PLANE('',#6041);
#5310=ADVANCED_FACE('',(#898,#168),#76,.T.);
#5311=ADVANCED_FACE('',(#899),#70,.F.);
#5312=ADVANCED_FACE('',(#900),#5000,.F.);
#5349=CLOSED_SHELL('',(#5310,#5311,#5312));
#6035=AXIS2_PLACEMENT_3D('',#9716,#7618,#7619);
#6036=AXIS2_PLACEMENT_3D('',#9717,#7620,#7621);
#6037=AXIS2_PLACEMENT_3D('',#9719,#7622,#7623);
#6038=AXIS2_PLACEMENT_3D('',#9720,#7624,#7625);
#6039=AXIS2_PLACEMENT_3D('',#9723,#7626,#7627);
#6040=AXIS2_PLACEMENT_3D('',#10250,#7628,#7629);
#6041=AXIS2_PLACEMENT_3D('',#10251,#7630,#7631);
#7618=DIRECTION('axis',(0.,0.,1.));
#7619=DIRECTION('refdir',(1.,0.,0.));
#7620=DIRECTION('center_axis',(2.22044604925031E-16,-1.,-1.22464679914735E-16));
#7621=DIRECTION('ref_axis',(0.,0.,-1.));
#7622=DIRECTION('center_axis',(-1.,-2.22044604925031E-16,0.));
#7623=DIRECTION('ref_axis',(0.,0.,1.));
#7624=DIRECTION('center_axis',(2.22044604925031E-16,-1.,-1.22464679914735E-16));
#7625=DIRECTION('ref_axis',(-2.71926214689378E-32,1.22464679914735E-16,
-1.));
#7626=DIRECTION('center_axis',(-1.,-2.22044604925031E-16,-2.71926214689378E-32));
#7627=DIRECTION('ref_axis',(-2.22044604925031E-16,1.,1.22464679914735E-16));
#7628=DIRECTION('center_axis',(1.,-1.00260219422232E-15,-1.22783356797248E-31));
#7629=DIRECTION('ref_axis',(1.00260219422232E-15,1.,1.22464679914735E-16));
#7630=DIRECTION('center_axis',(1.,-1.00260219422232E-15,-1.22783356797248E-31));
#7631=DIRECTION('ref_axis',(0.,1.22464679914735E-16,-1.));
#9716=CARTESIAN_POINT('',(0.,0.,0.));
#9717=CARTESIAN_POINT('Origin',(-10.9359120418715,26.3504782148047,17.6));
#9718=CARTESIAN_POINT('',(-10.9359120418715,26.3504782148047,18.35));
#9719=CARTESIAN_POINT('Origin',(-10.9359120418715,26.3504782148047,18.6));
#9720=CARTESIAN_POINT('Origin',(-10.9359120418715,26.3504782148047,17.6));
#9721=CARTESIAN_POINT('',(-10.9359120418715,26.6004782148047,16.6));
#9722=CARTESIAN_POINT('',(-10.9359120418715,26.1004782148047,16.6));
#9723=CARTESIAN_POINT('Origin',(-10.9359120418715,26.3504782148047,16.6));
#9724=CARTESIAN_POINT('Ctrl Pts',(-10.9359120418715,26.6004782148047,16.6));
#9725=CARTESIAN_POINT('Ctrl Pts',(-10.9402193353539,26.6004782148047,16.5977092724426));
#9726=CARTESIAN_POINT('Ctrl Pts',(-10.9445589464746,26.6004467587024,16.5954788663774));
#9727=CARTESIAN_POINT('Ctrl Pts',(-10.9872540124717,26.5998563522904,16.5742560748851));
#9728=CARTESIAN_POINT('Ctrl Pts',(-11.0283064246552,26.5971771315259,16.559542959919));
#9729=CARTESIAN_POINT('Ctrl Pts',(-11.0701108612612,26.5930900009076,16.5481972195909));
#9730=CARTESIAN_POINT('Ctrl Pts',(-11.0708339684841,26.5930188703742,16.5480020646239));
#9731=CARTESIAN_POINT('Ctrl Pts',(-11.0827759229911,26.5918370097103,16.544797109728));
#9732=CARTESIAN_POINT('Ctrl Pts',(-11.094063293504,26.590615824153,16.5420298581508));
#9733=CARTESIAN_POINT('Ctrl Pts',(-11.110070277255,26.5887362807543,16.5384418503857));
#9734=CARTESIAN_POINT('Ctrl Pts',(-11.1147727349573,26.5881661562854,16.5374286265409));
#9735=CARTESIAN_POINT('Ctrl Pts',(-11.1230847074372,26.5871263380585,16.5357072275207));
#9736=CARTESIAN_POINT('Ctrl Pts',(-11.1266932353496,26.5866642710644,16.5349829852478));
#9737=CARTESIAN_POINT('Ctrl Pts',(-11.1343464784642,26.585661455081,16.5334946079531));
#9738=CARTESIAN_POINT('Ctrl Pts',(-11.1383928290144,26.5851177664648,16.5327358435474));
#9739=CARTESIAN_POINT('Ctrl Pts',(-11.1481733797635,26.5837704893605,16.5309679692519));
#9740=CARTESIAN_POINT('Ctrl Pts',(-11.1539124540547,26.5829524731398,16.5299854641958));
#9741=CARTESIAN_POINT('Ctrl Pts',(-11.1737387918633,26.5800291593595,16.5267739133408));
#9742=CARTESIAN_POINT('Ctrl Pts',(-11.1878669666236,26.577776425181,16.5248034466825));
#9743=CARTESIAN_POINT('Ctrl Pts',(-11.2400872187947,26.568769854808,16.5186110231589));
#9744=CARTESIAN_POINT('Ctrl Pts',(-11.2785053382042,26.5608013780416,16.5162061142361));
#9745=CARTESIAN_POINT('Ctrl Pts',(-11.3413563804704,26.5448431161272,16.5154725363415));
#9746=CARTESIAN_POINT('Ctrl Pts',(-11.3663341463412,26.5377137973801,16.5160451884648));
#9747=CARTESIAN_POINT('Ctrl Pts',(-11.4675067236831,26.5048705240401,16.5219235534991));
#9748=CARTESIAN_POINT('Ctrl Pts',(-11.5339527175624,26.4736908333921,16.5341985199053));
#9749=CARTESIAN_POINT('Ctrl Pts',(-11.6275973319121,26.408664050569,16.5639151059098));
#9750=CARTESIAN_POINT('Ctrl Pts',(-11.6584745098273,26.3779628401158,16.5791986989673));
#9751=CARTESIAN_POINT('Ctrl Pts',(-11.693043062557,26.3250017138209,16.605627659773));
#9752=CARTESIAN_POINT('Ctrl Pts',(-11.7019011653722,26.3029596082007,16.6166575639151));
#9753=CARTESIAN_POINT('Ctrl Pts',(-11.7077448592175,26.2652062478922,16.6350648852536));
#9754=CARTESIAN_POINT('Ctrl Pts',(-11.7070741798815,26.2486012355755,16.6429988757827));
#9755=CARTESIAN_POINT('Ctrl Pts',(-11.698268450351,26.2180039204305,16.6569651923278));
#9756=CARTESIAN_POINT('Ctrl Pts',(-11.6911945436197,26.2046479601392,16.6627780404676));
#9757=CARTESIAN_POINT('Ctrl Pts',(-11.6706730422176,26.1789460999401,16.6732083185761));
#9758=CARTESIAN_POINT('Ctrl Pts',(-11.6571316130369,26.1675135294197,16.677362768157));
#9759=CARTESIAN_POINT('Ctrl Pts',(-11.6199753453774,26.1438724951594,16.6848437491615));
#9760=CARTESIAN_POINT('Ctrl Pts',(-11.5946921404572,26.1337519058654,16.686910649375));
#9761=CARTESIAN_POINT('Ctrl Pts',(-11.5217072854985,26.1124320719796,16.6888104810606));
#9762=CARTESIAN_POINT('Ctrl Pts',(-11.4671883817412,26.1060347853434,16.6853604690573));
#9763=CARTESIAN_POINT('Ctrl Pts',(-11.2981182229277,26.0969290280957,16.6690502405298));
#9764=CARTESIAN_POINT('Ctrl Pts',(-11.0857203861473,26.1008383327785,16.6427595546923));
#9765=CARTESIAN_POINT('Ctrl Pts',(-10.941103632581,26.1004816814786,16.6015112866721));
#9766=CARTESIAN_POINT('Ctrl Pts',(-10.9385065750259,26.1004782148047,16.6007604391535));
#9767=CARTESIAN_POINT('Ctrl Pts',(-10.9359120418715,26.1004782148047,16.6));
#9768=CARTESIAN_POINT('Ctrl Pts',(-10.9359120418715,26.1004782148047,16.6));
#9769=CARTESIAN_POINT('Ctrl Pts',(-11.099536659246,26.1004782148047,16.553125));
#9770=CARTESIAN_POINT('Ctrl Pts',(-11.425478146952,26.0179944258633,16.459375));
#9771=CARTESIAN_POINT('Ctrl Pts',(-11.9300789153048,25.5673438360005,16.271875));
#9772=CARTESIAN_POINT('Ctrl Pts',(-12.0229540626903,24.6519632977172,16.0375));
#9773=CARTESIAN_POINT('Ctrl Pts',(-11.164885722509,23.9466553694149,15.75625));
#9774=CARTESIAN_POINT('Ctrl Pts',(-10.1047480288197,24.2694595959893,15.475));
#9775=CARTESIAN_POINT('Ctrl Pts',(-9.7826825635668,25.329679981508,15.19375));
#9776=CARTESIAN_POINT('Ctrl Pts',(-10.4860312388173,26.1867889046978,14.9125));
#9777=CARTESIAN_POINT('Ctrl Pts',(-11.5890842776128,26.0780137287588,14.63125));
#9778=CARTESIAN_POINT('Ctrl Pts',(-12.1116466665383,25.1004991337717,14.35));
#9779=CARTESIAN_POINT('Ctrl Pts',(-11.5891025224479,24.1228902184961,14.06875));
#9780=CARTESIAN_POINT('Ctrl Pts',(-10.4859854650458,24.0142573573597,13.7875));
#9781=CARTESIAN_POINT('Ctrl Pts',(-9.78277916381912,24.8711035465199,13.50625));
#9782=CARTESIAN_POINT('Ctrl Pts',(-10.1045513655818,25.9318409055902,13.225));
#9783=CARTESIAN_POINT('Ctrl Pts',(-11.1652837785312,26.2536089704377,12.94375));
#9784=CARTESIAN_POINT('Ctrl Pts',(-12.0221382397948,25.5504081019422,12.6625));
#9785=CARTESIAN_POINT('Ctrl Pts',(-11.9134895714075,24.4472815516099,12.38125));
#9786=CARTESIAN_POINT('Ctrl Pts',(-10.9359120418715,23.9247557910194,12.1));
#9787=CARTESIAN_POINT('Ctrl Pts',(-9.95833451233548,24.4472815516099,11.81875));
#9788=CARTESIAN_POINT('Ctrl Pts',(-9.84968584394817,25.5504081019422,11.5375));
#9789=CARTESIAN_POINT('Ctrl Pts',(-10.7065403052118,26.2536089704376,11.25625));
#9790=CARTESIAN_POINT('Ctrl Pts',(-11.7672727181612,25.9318409055902,10.975));
#9791=CARTESIAN_POINT('Ctrl Pts',(-12.0890449199239,24.8711035465198,10.69375));
#9792=CARTESIAN_POINT('Ctrl Pts',(-11.3858386186972,24.0142573573597,10.4125));
#9793=CARTESIAN_POINT('Ctrl Pts',(-10.2827215612951,24.1228902184961,10.13125));
#9794=CARTESIAN_POINT('Ctrl Pts',(-9.76017741720471,25.1004991337717,9.85000000000001));
#9795=CARTESIAN_POINT('Ctrl Pts',(-10.2827398061301,26.0780137287587,9.56874999999999));
#9796=CARTESIAN_POINT('Ctrl Pts',(-11.3857928449257,26.1867889046978,9.28750000000001));
#9797=CARTESIAN_POINT('Ctrl Pts',(-12.0891415201762,25.329679981508,9.00624999999999));
#9798=CARTESIAN_POINT('Ctrl Pts',(-11.7670760549233,24.2694595959893,8.725));
#9799=CARTESIAN_POINT('Ctrl Pts',(-10.706938361234,23.946655369415,8.44375));
#9800=CARTESIAN_POINT('Ctrl Pts',(-9.84887002105266,24.6519632977172,8.1625));
#9801=CARTESIAN_POINT('Ctrl Pts',(-9.9417451684382,25.5673438360005,7.92812499999999));
#9802=CARTESIAN_POINT('Ctrl Pts',(-10.446345936791,26.0179944258633,7.740625));
#9803=CARTESIAN_POINT('Ctrl Pts',(-10.772287424497,26.1004782148047,7.646875));
#9804=CARTESIAN_POINT('Ctrl Pts',(-10.9359120418715,26.1004782148047,7.6));
#9805=CARTESIAN_POINT('Ctrl Pts',(-10.9359120418715,26.1004782148047,16.5439001311859));
#9806=CARTESIAN_POINT('Ctrl Pts',(-11.0994822304736,26.1004782148047,16.4970251311859));
#9807=CARTESIAN_POINT('Ctrl Pts',(-11.4254856552641,26.0179777379893,16.4032751311859));
#9808=CARTESIAN_POINT('Ctrl Pts',(-11.9299950149165,25.5673798144889,16.2157751311859));
#9809=CARTESIAN_POINT('Ctrl Pts',(-12.0229600596387,24.6519505470442,15.9814001311859));
#9810=CARTESIAN_POINT('Ctrl Pts',(-11.1648652565317,23.946693336158,15.7001501311859));
#9811=CARTESIAN_POINT('Ctrl Pts',(-10.1047747807049,24.2694732685672,15.4189001311859));
#9812=CARTESIAN_POINT('Ctrl Pts',(-9.78270553499417,25.3296774410397,15.1376501311859));
#9813=CARTESIAN_POINT('Ctrl Pts',(-10.4860435089969,26.1867623778528,14.8564001311859));
#9814=CARTESIAN_POINT('Ctrl Pts',(-11.5890682328979,26.0779917788703,14.5751501311859));
#9815=CARTESIAN_POINT('Ctrl Pts',(-12.1116199022434,25.1004987935522,14.2939001311859));
#9816=CARTESIAN_POINT('Ctrl Pts',(-11.5890871711374,24.1229130219417,14.0126501311859));
#9817=CARTESIAN_POINT('Ctrl Pts',(-10.4859959955657,24.014282423191,13.7314001311859));
#9818=CARTESIAN_POINT('Ctrl Pts',(-9.7828058066508,24.8711088991058,13.4501501311859));
#9819=CARTESIAN_POINT('Ctrl Pts',(-10.1045706423353,25.9318216358326,13.1689001311859));
#9820=CARTESIAN_POINT('Ctrl Pts',(-11.1652784540862,26.2535822819133,12.8876501311859));
#9821=CARTESIAN_POINT('Ctrl Pts',(-12.0221130963663,25.5503976790619,12.6064001311859));
#9822=CARTESIAN_POINT('Ctrl Pts',(-11.9134669344998,24.4472966785626,12.3251501311859));
#9823=CARTESIAN_POINT('Ctrl Pts',(-10.9359120418715,23.9247830105523,12.0439001311859));
#9824=CARTESIAN_POINT('Ctrl Pts',(-9.95835714924316,24.4472966785625,11.7626501311859));
#9825=CARTESIAN_POINT('Ctrl Pts',(-9.84971098737667,25.5503976790619,11.4814001311859));
#9826=CARTESIAN_POINT('Ctrl Pts',(-10.7065456296568,26.2535822819133,11.2001501311859));
#9827=CARTESIAN_POINT('Ctrl Pts',(-11.7672534414077,25.9318216358326,10.9189001311859));
#9828=CARTESIAN_POINT('Ctrl Pts',(-12.0890182770922,24.8711088991058,10.6376501311859));
#9829=CARTESIAN_POINT('Ctrl Pts',(-11.3858280881773,24.014282423191,10.3564001311859));
#9830=CARTESIAN_POINT('Ctrl Pts',(-10.2827369126056,24.1229130219416,10.0751501311859));
#9831=CARTESIAN_POINT('Ctrl Pts',(-9.76020418149962,25.1004987935522,9.7939001311859));
#9832=CARTESIAN_POINT('Ctrl Pts',(-10.2827558508451,26.0779917788702,9.5126501311859));
#9833=CARTESIAN_POINT('Ctrl Pts',(-11.3857805747461,26.1867623778528,9.23140013118589));
#9834=CARTESIAN_POINT('Ctrl Pts',(-12.0891185487488,25.3296774410397,8.9501501311859));
#9835=CARTESIAN_POINT('Ctrl Pts',(-11.7670493030381,24.2694732685672,8.66890013118588));
#9836=CARTESIAN_POINT('Ctrl Pts',(-10.7069588272113,23.946693336158,8.38765013118591));
#9837=CARTESIAN_POINT('Ctrl Pts',(-9.84886402410427,24.6519505470442,8.10640013118589));
#9838=CARTESIAN_POINT('Ctrl Pts',(-9.94182906882648,25.5673798144889,7.8720251311859));
#9839=CARTESIAN_POINT('Ctrl Pts',(-10.4463384284789,26.0179777379893,7.6845251311859));
#9840=CARTESIAN_POINT('Ctrl Pts',(-10.7723418532693,26.1004782148047,7.5907751311859));
#9841=CARTESIAN_POINT('Ctrl Pts',(-10.9359120418715,26.1004782148047,7.5439001311859));
#9842=CARTESIAN_POINT('Ctrl Pts',(-10.9359120418715,26.1266450098064,16.4693527133209));
#9843=CARTESIAN_POINT('Ctrl Pts',(-11.1038344518235,26.1266450098064,16.4224777133209));
#9844=CARTESIAN_POINT('Ctrl Pts',(-11.4382862797329,26.0420078700208,16.3287277133209));
#9845=CARTESIAN_POINT('Ctrl Pts',(-11.9561181415698,25.5795494643233,16.1412277133209));
#9846=CARTESIAN_POINT('Ctrl Pts',(-12.0513966768011,24.640230909128,15.9068527133209));
#9847=CARTESIAN_POINT('Ctrl Pts',(-11.1708833441426,23.9164521808741,15.6256027133209));
#9848=CARTESIAN_POINT('Ctrl Pts',(-10.0829911382721,24.247710417425,15.3443527133209));
#9849=CARTESIAN_POINT('Ctrl Pts',(-9.75249938143592,25.3356782161237,15.0631027133209));
#9850=CARTESIAN_POINT('Ctrl Pts',(-10.4742556343159,26.2152220988022,14.7818527133209));
#9851=CARTESIAN_POINT('Ctrl Pts',(-11.6061804950126,26.1035992577537,14.5006027133209));
#9852=CARTESIAN_POINT('Ctrl Pts',(-12.142419869351,25.1004997827956,14.2193527133209));
#9853=CARTESIAN_POINT('Ctrl Pts',(-11.6061990100998,24.0973030612035,13.9381027133209));
#9854=CARTESIAN_POINT('Ctrl Pts',(-10.4742091825201,23.9858269503648,13.6568527133209));
#9855=CARTESIAN_POINT('Ctrl Pts',(-9.75259741256427,24.8650999474953,13.3756027133209));
#9856=CARTESIAN_POINT('Ctrl Pts',(-10.0827915622055,25.9536007595893,13.0943527133209));
#9857=CARTESIAN_POINT('Ctrl Pts',(-11.1712872924373,26.2837906798065,12.8131027133209));
#9858=CARTESIAN_POINT('Ctrl Pts',(-12.0505688097153,25.5621844389304,12.5318527133209));
#9859=CARTESIAN_POINT('Ctrl Pts',(-11.9390764050646,24.4301849692063,12.2506027133209));
#9860=CARTESIAN_POINT('Ctrl Pts',(-10.9359120418715,23.8939827714609,11.9693527133209));
#9861=CARTESIAN_POINT('Ctrl Pts',(-9.93274767867843,24.4301849692063,11.6881027133209));
#9862=CARTESIAN_POINT('Ctrl Pts',(-9.82125527402764,25.5621844389305,11.4068527133209));
#9863=CARTESIAN_POINT('Ctrl Pts',(-10.7005367913057,26.2837906798064,11.1256027133209));
#9864=CARTESIAN_POINT('Ctrl Pts',(-11.7890325215375,25.9536007595894,10.8443527133209));
#9865=CARTESIAN_POINT('Ctrl Pts',(-12.1192266711787,24.8650999474953,10.5631027133209));
#9866=CARTESIAN_POINT('Ctrl Pts',(-11.3976149012229,23.9858269503648,10.2818527133209));
#9867=CARTESIAN_POINT('Ctrl Pts',(-10.2656250736432,24.0973030612034,10.0006027133209));
#9868=CARTESIAN_POINT('Ctrl Pts',(-9.72940421439204,25.1004997827956,9.7193527133209));
#9869=CARTESIAN_POINT('Ctrl Pts',(-10.2656435887304,26.1035992577537,9.43810271332087));
#9870=CARTESIAN_POINT('Ctrl Pts',(-11.3975684494271,26.2152220988022,9.1568527133209));
#9871=CARTESIAN_POINT('Ctrl Pts',(-12.1193247023071,25.3356782161237,8.87560271332088));
#9872=CARTESIAN_POINT('Ctrl Pts',(-11.7888329454709,24.2477104174249,8.59435271332089));
#9873=CARTESIAN_POINT('Ctrl Pts',(-10.7009407396004,23.9164521808741,8.31310271332088));
#9874=CARTESIAN_POINT('Ctrl Pts',(-9.82042740694183,24.640230909128,8.03185271332089));
#9875=CARTESIAN_POINT('Ctrl Pts',(-9.91570594217325,25.5795494643233,7.79747771332088));
#9876=CARTESIAN_POINT('Ctrl Pts',(-10.4335378040101,26.0420078700208,7.60997771332088));
#9877=CARTESIAN_POINT('Ctrl Pts',(-10.7679896319195,26.1266450098064,7.51622771332088));
#9878=CARTESIAN_POINT('Ctrl Pts',(-10.9359120418715,26.1266450098064,7.46935271332088));
#9879=CARTESIAN_POINT('Ctrl Pts',(-10.9359120418715,26.2066161778899,16.3896589751759));
#9880=CARTESIAN_POINT('Ctrl Pts',(-11.1168911197771,26.2066161778899,16.3427839751759));
#9881=CARTESIAN_POINT('Ctrl Pts',(-11.477441396077,26.1153739493474,16.2490339751759));
#9882=CARTESIAN_POINT('Ctrl Pts',(-12.0355787665632,25.6169041478587,16.0615339751759));
#9883=CARTESIAN_POINT('Ctrl Pts',(-12.1383318463205,24.6043559511596,15.8271589751759));
#9884=CARTESIAN_POINT('Ctrl Pts',(-11.1891838889267,23.8241995587892,15.5459089751759));
#9885=CARTESIAN_POINT('Ctrl Pts',(-10.0165360303049,24.1812600680729,15.2646589751759));
#9886=CARTESIAN_POINT('Ctrl Pts',(-9.66028633666698,25.354006414981,14.9834089751759));
#9887=CARTESIAN_POINT('Ctrl Pts',(-10.4382845848074,26.3020817027312,14.7021589751759));
#9888=CARTESIAN_POINT('Ctrl Pts',(-11.6584070156187,26.1817623874398,14.4209089751759));
#9889=CARTESIAN_POINT('Ctrl Pts',(-12.2364306850993,25.1005012770401,14.1396589751759));
#9890=CARTESIAN_POINT('Ctrl Pts',(-11.6584273539152,24.0191361826963,13.8584089751759));
#9891=CARTESIAN_POINT('Ctrl Pts',(-10.4382335588295,23.8989737631753,13.5771589751759));
#9892=CARTESIAN_POINT('Ctrl Pts',(-9.66039402110579,24.8467593983089,13.2959089751759));
#9893=CARTESIAN_POINT('Ctrl Pts',(-10.0163168012077,26.0200756853628,13.0146589751759));
#9894=CARTESIAN_POINT('Ctrl Pts',(-11.1896276219567,26.3759938775365,12.7334089751759));
#9895=CARTESIAN_POINT('Ctrl Pts',(-12.1374223832382,25.5981603838786,12.4521589751759));
#9896=CARTESIAN_POINT('Ctrl Pts',(-12.0172425339907,24.3779560131358,12.1709089751759));
#9897=CARTESIAN_POINT('Ctrl Pts',(-10.9359120418715,23.7999731705043,11.8896589751759));
#9898=CARTESIAN_POINT('Ctrl Pts',(-9.85458154975225,24.3779560131359,11.6084089751759));
#9899=CARTESIAN_POINT('Ctrl Pts',(-9.73440170050483,25.5981603838786,11.3271589751759));
#9900=CARTESIAN_POINT('Ctrl Pts',(-10.6821964617862,26.3759938775366,11.0459089751759));
#9901=CARTESIAN_POINT('Ctrl Pts',(-11.8555072825353,26.0200756853628,10.7646589751759));
#9902=CARTESIAN_POINT('Ctrl Pts',(-12.2114300626372,24.8467593983089,10.4834089751759));
#9903=CARTESIAN_POINT('Ctrl Pts',(-11.4335905249135,23.8989737631753,10.2021589751759));
#9904=CARTESIAN_POINT('Ctrl Pts',(-10.2133967298278,24.0191361826963,9.92090897517594));
#9905=CARTESIAN_POINT('Ctrl Pts',(-9.63539339864373,25.1005012770401,9.63965897517594));
#9906=CARTESIAN_POINT('Ctrl Pts',(-10.2134170681242,26.1817623874398,9.35840897517593));
#9907=CARTESIAN_POINT('Ctrl Pts',(-11.4335394989356,26.3020817027312,9.07715897517594));
#9908=CARTESIAN_POINT('Ctrl Pts',(-12.211537747076,25.354006414981,8.79590897517593));
#9909=CARTESIAN_POINT('Ctrl Pts',(-11.8552880534381,24.1812600680728,8.51465897517594));
#9910=CARTESIAN_POINT('Ctrl Pts',(-10.6826401948163,23.8241995587893,8.23340897517593));
#9911=CARTESIAN_POINT('Ctrl Pts',(-9.73349223742245,24.6043559511596,7.95215897517595));
#9912=CARTESIAN_POINT('Ctrl Pts',(-9.83624531717977,25.6169041478587,7.71778397517593));
#9913=CARTESIAN_POINT('Ctrl Pts',(-10.394382687666,26.1153739493474,7.53028397517594));
#9914=CARTESIAN_POINT('Ctrl Pts',(-10.7549329639659,26.2066161778899,7.43653397517594));
#9915=CARTESIAN_POINT('Ctrl Pts',(-10.9359120418715,26.2066161778899,7.38965897517594));
#9916=CARTESIAN_POINT('Ctrl Pts',(-10.9359120418715,26.3102987264096,16.3393291535573));
#9917=CARTESIAN_POINT('Ctrl Pts',(-11.1338720637509,26.3102987264096,16.2924541535573));
#9918=CARTESIAN_POINT('Ctrl Pts',(-11.5281986604801,26.2105092515307,16.1987041535573));
#9919=CARTESIAN_POINT('Ctrl Pts',(-12.1386810721185,25.6652994374558,16.0112041535573));
#9920=CARTESIAN_POINT('Ctrl Pts',(-12.2510373785934,24.5578565125378,15.7768291535573));
#9921=CARTESIAN_POINT('Ctrl Pts',(-11.2129304523193,23.7045571560224,15.4955791535573));
#9922=CARTESIAN_POINT('Ctrl Pts',(-9.93035099920634,24.0950939390133,15.2143291535573));
#9923=CARTESIAN_POINT('Ctrl Pts',(-9.54070984355737,25.3777713816557,14.9330791535573));
#9924=CARTESIAN_POINT('Ctrl Pts',(-10.3916362061851,26.414720925681,14.6518291535573));
#9925=CARTESIAN_POINT('Ctrl Pts',(-11.7261342725577,26.283122183649,14.3705791535573));
#9926=CARTESIAN_POINT('Ctrl Pts',(-12.3583416789862,25.1005035455251,14.0893291535573));
#9927=CARTESIAN_POINT('Ctrl Pts',(-11.726156299625,23.9177706952197,13.8080791535573));
#9928=CARTESIAN_POINT('Ctrl Pts',(-10.3915809433155,23.7863442817964,13.5268291535573));
#9929=CARTESIAN_POINT('Ctrl Pts',(-9.54082646945068,24.8229756818914,13.2455791535573));
#9930=CARTESIAN_POINT('Ctrl Pts',(-9.93011356689479,26.1062791264966,12.9643291535573));
#9931=CARTESIAN_POINT('Ctrl Pts',(-11.2134110261814,26.4955612225042,12.6830791535573));
#9932=CARTESIAN_POINT('Ctrl Pts',(-12.2500524410375,25.6448133111173,12.4018291535573));
#9933=CARTESIAN_POINT('Ctrl Pts',(-12.1186068875143,24.3102264920467,12.1205791535573));
#9934=CARTESIAN_POINT('Ctrl Pts',(-10.9359120418715,23.6780633084266,11.8393291535573));
#9935=CARTESIAN_POINT('Ctrl Pts',(-9.75321719622871,24.3102264920467,11.5580791535573));
#9936=CARTESIAN_POINT('Ctrl Pts',(-9.62177164270546,25.6448133111173,11.2768291535573));
#9937=CARTESIAN_POINT('Ctrl Pts',(-10.6584130575616,26.4955612225041,10.9955791535573));
#9938=CARTESIAN_POINT('Ctrl Pts',(-11.9417105168482,26.1062791264966,10.7143291535573));
#9939=CARTESIAN_POINT('Ctrl Pts',(-12.3309976142923,24.8229756818914,10.4330791535573));
#9940=CARTESIAN_POINT('Ctrl Pts',(-11.4802431404275,23.7863442817964,10.1518291535573));
#9941=CARTESIAN_POINT('Ctrl Pts',(-10.1456677841179,23.9177706952197,9.8705791535573));
#9942=CARTESIAN_POINT('Ctrl Pts',(-9.51348240475674,25.100503545525,9.58932915355731));
#9943=CARTESIAN_POINT('Ctrl Pts',(-10.1456898111852,26.283122183649,9.30807915355731));
#9944=CARTESIAN_POINT('Ctrl Pts',(-11.4801878775579,26.414720925681,9.0268291535573));
#9945=CARTESIAN_POINT('Ctrl Pts',(-12.3311142401856,25.3777713816556,8.74557915355731));
#9946=CARTESIAN_POINT('Ctrl Pts',(-11.9414730845367,24.0950939390133,8.4643291535573));
#9947=CARTESIAN_POINT('Ctrl Pts',(-10.6588936314237,23.7045571560224,8.18307915355731));
#9948=CARTESIAN_POINT('Ctrl Pts',(-9.62078670514964,24.5578565125378,7.9018291535573));
#9949=CARTESIAN_POINT('Ctrl Pts',(-9.73314301162452,25.6652994374557,7.66745415355731));
#9950=CARTESIAN_POINT('Ctrl Pts',(-10.3436254232628,26.2105092515307,7.4799541535573));
#9951=CARTESIAN_POINT('Ctrl Pts',(-10.7379520199921,26.3102987264096,7.3862041535573));
#9952=CARTESIAN_POINT('Ctrl Pts',(-10.9359120418715,26.3102987264096,7.3393291535573));
#9953=CARTESIAN_POINT('Ctrl Pts',(-10.9359120418715,26.4672083419587,16.3570635515172));
#9954=CARTESIAN_POINT('Ctrl Pts',(-11.1595402772042,26.4672083419587,16.3101885515172));
#9955=CARTESIAN_POINT('Ctrl Pts',(-11.6050171261006,26.3544745087491,16.2164385515172));
#9956=CARTESIAN_POINT('Ctrl Pts',(-12.2946660690771,25.7385591499254,16.0289385515172));
#9957=CARTESIAN_POINT('Ctrl Pts',(-12.4216053921143,24.4874787891417,15.7945635515172));
#9958=CARTESIAN_POINT('Ctrl Pts',(-11.2488563449896,23.5235154857298,15.5133135515172));
#9959=CARTESIAN_POINT('Ctrl Pts',(-9.79993635312278,23.9647006498918,15.2320635515172));
#9960=CARTESIAN_POINT('Ctrl Pts',(-9.35975960806662,25.4137350597913,14.9508135515172));
#9961=CARTESIAN_POINT('Ctrl Pts',(-10.3210469490048,26.5851705638016,14.6695635515172));
#9962=CARTESIAN_POINT('Ctrl Pts',(-11.8286214898723,26.4365044605197,14.3883135515172));
#9963=CARTESIAN_POINT('Ctrl Pts',(-12.5428227658856,25.100506790018,14.1070635515172));
#9964=CARTESIAN_POINT('Ctrl Pts',(-11.828646456962,23.7643802784334,13.8258135515172));
#9965=CARTESIAN_POINT('Ctrl Pts',(-10.3209843100246,23.6159085765209,13.5445635515172));
#9966=CARTESIAN_POINT('Ctrl Pts',(-9.35989180039454,24.7869851870527,13.2633135515172));
#9967=CARTESIAN_POINT('Ctrl Pts',(-9.79966722986749,26.2367257803968,12.9820635515172));
#9968=CARTESIAN_POINT('Ctrl Pts',(-11.2494010641543,26.676495553443,12.7008135515172));
#9969=CARTESIAN_POINT('Ctrl Pts',(-12.4204889756426,25.715410475817,12.4195635515172));
#9970=CARTESIAN_POINT('Ctrl Pts',(-12.2719956805126,24.2077353396082,12.1383135515172));
#9971=CARTESIAN_POINT('Ctrl Pts',(-10.9359120418715,23.4935841866678,11.8570635515172));
#9972=CARTESIAN_POINT('Ctrl Pts',(-9.59982840323043,24.2077353396082,11.5758135515172));
#9973=CARTESIAN_POINT('Ctrl Pts',(-9.45133510810041,25.715410475817,11.2945635515172));
#9974=CARTESIAN_POINT('Ctrl Pts',(-10.6224230195887,26.676495553443,11.0133135515172));
#9975=CARTESIAN_POINT('Ctrl Pts',(-12.0721568538755,26.2367257803968,10.7320635515172));
#9976=CARTESIAN_POINT('Ctrl Pts',(-12.5119322833484,24.7869851870527,10.4508135515172));
#9977=CARTESIAN_POINT('Ctrl Pts',(-11.5508397737184,23.6159085765208,10.1695635515172));
#9978=CARTESIAN_POINT('Ctrl Pts',(-10.043177626781,23.7643802784334,9.88831355151715));
#9979=CARTESIAN_POINT('Ctrl Pts',(-9.32900131785735,25.100506790018,9.60706355151718));
#9980=CARTESIAN_POINT('Ctrl Pts',(-10.0432025938707,26.4365044605196,9.32581355151715));
#9981=CARTESIAN_POINT('Ctrl Pts',(-11.5507771347382,26.5851705638017,9.04456355151718));
#9982=CARTESIAN_POINT('Ctrl Pts',(-12.5120644756764,25.4137350597913,8.76331355151716));
#9983=CARTESIAN_POINT('Ctrl Pts',(-12.0718877306202,23.9647006498918,8.48206355151717));
#9984=CARTESIAN_POINT('Ctrl Pts',(-10.6229677387534,23.5235154857298,8.20081355151717));
#9985=CARTESIAN_POINT('Ctrl Pts',(-9.45021869162864,24.4874787891416,7.91956355151716));
#9986=CARTESIAN_POINT('Ctrl Pts',(-9.57715801466589,25.7385591499254,7.68518855151717));
#9987=CARTESIAN_POINT('Ctrl Pts',(-10.2668069576424,26.3544745087491,7.49768855151717));
#9988=CARTESIAN_POINT('Ctrl Pts',(-10.7122838065388,26.4672083419587,7.40393855151717));
#9989=CARTESIAN_POINT('Ctrl Pts',(-10.9359120418715,26.4672083419587,7.35706355151717));
#9990=CARTESIAN_POINT('Ctrl Pts',(-10.9359120418715,26.6081512188429,16.4968351856384));
#9991=CARTESIAN_POINT('Ctrl Pts',(-11.1825974273318,26.6081512188429,16.4499601856384));
#9992=CARTESIAN_POINT('Ctrl Pts',(-11.6740186123714,26.4837904806807,16.3562101856384));
#9993=CARTESIAN_POINT('Ctrl Pts',(-12.4347797573637,25.8043635573141,16.1687101856384));
#9994=CARTESIAN_POINT('Ctrl Pts',(-12.5748167258039,24.4242627348399,15.9343351856384));
#9995=CARTESIAN_POINT('Ctrl Pts',(-11.2811268343162,23.3608955651971,15.6530851856383));
#9996=CARTESIAN_POINT('Ctrl Pts',(-9.68279195417932,23.8475756440501,15.3718351856384));
#9997=CARTESIAN_POINT('Ctrl Pts',(-9.1972220581971,25.4460392026774,15.0905851856384));
#9998=CARTESIAN_POINT('Ctrl Pts',(-10.2576404855488,26.7382760883188,14.8093351856384));
#9999=CARTESIAN_POINT('Ctrl Pts',(-11.9206801154866,26.5742792834522,14.5280851856384));
#10000=CARTESIAN_POINT('Ctrl Pts',(-12.7085319370769,25.1005097098055,14.2468351856384));
#10001=CARTESIAN_POINT('Ctrl Pts',(-11.9207077123293,23.6265981302194,13.9655851856384));
#10002=CARTESIAN_POINT('Ctrl Pts',(-10.2575712488811,23.4628155904643,13.6843351856384));
#10003=CARTESIAN_POINT('Ctrl Pts',(-9.19736817418599,24.7546569112497,13.4030851856384));
#10004=CARTESIAN_POINT('Ctrl Pts',(-9.68249448443413,26.3538988103469,13.1218351856384));
#10005=CARTESIAN_POINT('Ctrl Pts',(-11.2817289291307,26.8390188766716,12.8405851856384));
#10006=CARTESIAN_POINT('Ctrl Pts',(-12.5735827078803,25.7788240125713,12.5593351856384));
#10007=CARTESIAN_POINT('Ctrl Pts',(-12.4097763675053,24.1156731939899,12.2780851856384));
#10008=CARTESIAN_POINT('Ctrl Pts',(-10.9359120418715,23.3278767733619,11.9968351856384));
#10009=CARTESIAN_POINT('Ctrl Pts',(-9.46204771623775,24.1156731939899,11.7155851856384));
#10010=CARTESIAN_POINT('Ctrl Pts',(-9.29824137586269,25.7788240125713,11.4343351856384));
#10011=CARTESIAN_POINT('Ctrl Pts',(-10.5900951546124,26.8390188766716,11.1530851856384));
#10012=CARTESIAN_POINT('Ctrl Pts',(-12.1893295993088,26.3538988103469,10.8718351856384));
#10013=CARTESIAN_POINT('Ctrl Pts',(-12.674455909557,24.7546569112497,10.5905851856384));
#10014=CARTESIAN_POINT('Ctrl Pts',(-11.6142528348618,23.4628155904642,10.3093351856384));
#10015=CARTESIAN_POINT('Ctrl Pts',(-9.95111637141368,23.6265981302195,10.0280851856384));
#10016=CARTESIAN_POINT('Ctrl Pts',(-9.16329214666605,25.1005097098054,9.74683518563837));
#10017=CARTESIAN_POINT('Ctrl Pts',(-9.9511439682564,26.5742792834522,9.46558518563839));
#10018=CARTESIAN_POINT('Ctrl Pts',(-11.6141835981942,26.7382760883188,9.18433518563837));
#10019=CARTESIAN_POINT('Ctrl Pts',(-12.6746020255459,25.4460392026774,8.90308518563838));
#10020=CARTESIAN_POINT('Ctrl Pts',(-12.1890321295637,23.8475756440501,8.62183518563838));
#10021=CARTESIAN_POINT('Ctrl Pts',(-10.5906972494268,23.3608955651972,8.34058518563839));
#10022=CARTESIAN_POINT('Ctrl Pts',(-9.29700735793908,24.4242627348399,8.05933518563838));
#10023=CARTESIAN_POINT('Ctrl Pts',(-9.43704432637928,25.8043635573141,7.82496018563839));
#10024=CARTESIAN_POINT('Ctrl Pts',(-10.1978054713715,26.4837904806807,7.63746018563838));
#10025=CARTESIAN_POINT('Ctrl Pts',(-10.6892266564112,26.6081512188429,7.54371018563838));
#10026=CARTESIAN_POINT('Ctrl Pts',(-10.9359120418715,26.6081512188429,7.49683518563838));
#10027=CARTESIAN_POINT('Ctrl Pts',(-10.9359120418715,26.6083071804768,16.7239284079399));
#10028=CARTESIAN_POINT('Ctrl Pts',(-11.1826417158169,26.6083071804768,16.6770534079399));
#10029=CARTESIAN_POINT('Ctrl Pts',(-11.6740923767204,26.4839393326867,16.5833034079399));
#10030=CARTESIAN_POINT('Ctrl Pts',(-12.4349637416248,25.8044239635482,16.3958034079399));
#10031=CARTESIAN_POINT('Ctrl Pts',(-12.5749841946544,24.4241971806872,16.1614284079399));
#10032=CARTESIAN_POINT('Ctrl Pts',(-11.2811696029524,23.3607025205763,15.8801784079399));
#10033=CARTESIAN_POINT('Ctrl Pts',(-9.68265309931028,23.8474413221505,15.5989284079399));
#10034=CARTESIAN_POINT('Ctrl Pts',(-9.19703427713218,25.4460758254194,15.3176784079399));
#10035=CARTESIAN_POINT('Ctrl Pts',(-10.2575660901313,26.7384546586772,15.0364284079399));
#10036=CARTESIAN_POINT('Ctrl Pts',(-11.9207875181861,26.5744393107299,14.7551784079399));
#10037=CARTESIAN_POINT('Ctrl Pts',(-12.7087245360209,25.10050983039,14.4739284079399));
#10038=CARTESIAN_POINT('Ctrl Pts',(-11.9208148787593,23.6264378004142,14.1926784079399));
#10039=CARTESIAN_POINT('Ctrl Pts',(-10.2574974462324,23.4626375379351,13.9114284079399));
#10040=CARTESIAN_POINT('Ctrl Pts',(-9.19717914213288,24.7546192918056,13.6301784079399));
#10041=CARTESIAN_POINT('Ctrl Pts',(-9.68235817663199,26.3540351160508,13.3489284079399));
#10042=CARTESIAN_POINT('Ctrl Pts',(-11.2817665384133,26.8392079241505,13.0676784079399));
#10043=CARTESIAN_POINT('Ctrl Pts',(-12.5737607880012,25.7788977786177,12.7864284079399));
#10044=CARTESIAN_POINT('Ctrl Pts',(-12.4099366382488,24.1155661039636,12.5051784079399));
#10045=CARTESIAN_POINT('Ctrl Pts',(-10.9359120418715,23.3276840193356,12.2239284079399));
#10046=CARTESIAN_POINT('Ctrl Pts',(-9.4618874454942,24.1155661039636,11.9426784079399));
#10047=CARTESIAN_POINT('Ctrl Pts',(-9.29806329574184,25.7788977786177,11.6614284079399));
#10048=CARTESIAN_POINT('Ctrl Pts',(-10.5900575453297,26.8392079241504,11.3801784079399));
#10049=CARTESIAN_POINT('Ctrl Pts',(-12.189465907111,26.3540351160508,11.0989284079399));
#10050=CARTESIAN_POINT('Ctrl Pts',(-12.6746449416101,24.7546192918055,10.8176784079399));
#10051=CARTESIAN_POINT('Ctrl Pts',(-11.6143266375106,23.4626375379351,10.5364284079399));
#10052=CARTESIAN_POINT('Ctrl Pts',(-9.95100920498365,23.6264378004142,10.2551784079399));
#10053=CARTESIAN_POINT('Ctrl Pts',(-9.16309954772204,25.10050983039,9.9739284079399));
#10054=CARTESIAN_POINT('Ctrl Pts',(-9.95103656555694,26.5744393107299,9.6926784079399));
#10055=CARTESIAN_POINT('Ctrl Pts',(-11.6142579936116,26.7384546586772,9.4114284079399));
#10056=CARTESIAN_POINT('Ctrl Pts',(-12.6747898066108,25.4460758254194,9.13017840793991));
#10057=CARTESIAN_POINT('Ctrl Pts',(-12.1891709844327,23.8474413221505,8.84892840793989));
#10058=CARTESIAN_POINT('Ctrl Pts',(-10.5906544807905,23.3607025205763,8.5676784079399));
#10059=CARTESIAN_POINT('Ctrl Pts',(-9.29683988908855,24.4241971806872,8.2864284079399));
#10060=CARTESIAN_POINT('Ctrl Pts',(-9.43686034211822,25.8044239635482,8.05205340793991));
#10061=CARTESIAN_POINT('Ctrl Pts',(-10.1977317070226,26.4839393326867,7.8645534079399));
#10062=CARTESIAN_POINT('Ctrl Pts',(-10.6891823679261,26.6083071804768,7.77080340793991));
#10063=CARTESIAN_POINT('Ctrl Pts',(-10.9359120418715,26.6083071804768,7.7239284079399));
#10064=CARTESIAN_POINT('Ctrl Pts',(-10.9359120418715,26.4141282398751,16.8792407663736));
#10065=CARTESIAN_POINT('Ctrl Pts',(-11.1508380894168,26.4141282398751,16.8323657663736));
#10066=CARTESIAN_POINT('Ctrl Pts',(-11.579033249117,26.3057674496366,16.7386157663736));
#10067=CARTESIAN_POINT('Ctrl Pts',(-12.2418694213241,25.7137890968229,16.5511157663736));
#10068=CARTESIAN_POINT('Ctrl Pts',(-12.3639069611349,24.5112820297777,16.3167407663736));
#10069=CARTESIAN_POINT('Ctrl Pts',(-11.2366960152862,23.5847723620182,16.0354907663736));
#10070=CARTESIAN_POINT('Ctrl Pts',(-9.8440629677261,24.0088154675039,15.7542407663736));
#10071=CARTESIAN_POINT('Ctrl Pts',(-9.4209803113142,25.4015682142421,15.4729907663736));
#10072=CARTESIAN_POINT('Ctrl Pts',(-10.3449304950388,26.5275008077356,15.1917407663736));
#10073=CARTESIAN_POINT('Ctrl Pts',(-11.7939460365568,26.3846099294544,14.9104907663736));
#10074=CARTESIAN_POINT('Ctrl Pts',(-12.4804063041722,25.1005055735222,14.6292407663736));
#10075=CARTESIAN_POINT('Ctrl Pts',(-11.7939702514824,23.8162778614928,14.3479907663736));
#10076=CARTESIAN_POINT('Ctrl Pts',(-10.3448697431333,23.6735731085796,14.0667407663736));
#10077=CARTESIAN_POINT('Ctrl Pts',(-9.42110852120592,24.7991620873381,13.7854907663736));
#10078=CARTESIAN_POINT('Ctrl Pts',(-9.84380195187374,26.192590953643,13.5042407663736));
#10079=CARTESIAN_POINT('Ctrl Pts',(-11.2372243282571,26.6152789310382,13.2229907663736));
#10080=CARTESIAN_POINT('Ctrl Pts',(-12.362824135908,25.6915249005696,12.9417407663736));
#10081=CARTESIAN_POINT('Ctrl Pts',(-12.2200987049739,24.2424118032843,12.6604907663736));
#10082=CARTESIAN_POINT('Ctrl Pts',(-10.9359120418715,23.5560001427465,12.3792407663736));
#10083=CARTESIAN_POINT('Ctrl Pts',(-9.65172537876912,24.2424118032843,12.0979907663736));
#10084=CARTESIAN_POINT('Ctrl Pts',(-9.50899994783496,25.6915249005695,11.8167407663736));
#10085=CARTESIAN_POINT('Ctrl Pts',(-10.6345997554859,26.6152789310382,11.5354907663736));
#10086=CARTESIAN_POINT('Ctrl Pts',(-12.0280221318692,26.192590953643,11.2542407663736));
#10087=CARTESIAN_POINT('Ctrl Pts',(-12.4507155625371,24.7991620873381,10.9729907663736));
#10088=CARTESIAN_POINT('Ctrl Pts',(-11.5269543406097,23.6735731085796,10.6917407663736));
#10089=CARTESIAN_POINT('Ctrl Pts',(-10.0778538322605,23.8162778614928,10.4104907663736));
#10090=CARTESIAN_POINT('Ctrl Pts',(-9.39141777957078,25.1005055735222,10.1292407663736));
#10091=CARTESIAN_POINT('Ctrl Pts',(-10.0778780471862,26.3846099294544,9.84799076637357));
#10092=CARTESIAN_POINT('Ctrl Pts',(-11.5268935887042,26.5275008077356,9.56674076637359));
#10093=CARTESIAN_POINT('Ctrl Pts',(-12.4508437724288,25.4015682142421,9.28549076637358));
#10094=CARTESIAN_POINT('Ctrl Pts',(-12.0277611160169,24.008815467504,9.00424076637358));
#10095=CARTESIAN_POINT('Ctrl Pts',(-10.6351280684568,23.5847723620182,8.72299076637358));
#10096=CARTESIAN_POINT('Ctrl Pts',(-9.5079171226081,24.5112820297778,8.44174076637358));
#10097=CARTESIAN_POINT('Ctrl Pts',(-9.62995466241886,25.7137890968229,8.20736576637358));
#10098=CARTESIAN_POINT('Ctrl Pts',(-10.292790834626,26.3057674496365,8.01986576637358));
#10099=CARTESIAN_POINT('Ctrl Pts',(-10.7209859943261,26.4141282398751,7.92611576637358));
#10100=CARTESIAN_POINT('Ctrl Pts',(-10.9359120418715,26.4141282398751,7.87924076637358));
#10101=CARTESIAN_POINT('Ctrl Pts',(-10.9359120418715,26.1720429125025,16.82358003041));
#10102=CARTESIAN_POINT('Ctrl Pts',(-11.1112963140765,26.1720429125025,16.77670503041));
#10103=CARTESIAN_POINT('Ctrl Pts',(-11.4605069125061,26.0836714981141,16.68295503041));
#10104=CARTESIAN_POINT('Ctrl Pts',(-12.0013030996622,25.6007219425128,16.49545503041));
#10105=CARTESIAN_POINT('Ctrl Pts',(-12.1007423973834,24.6198771550135,16.26108003041));
#10106=CARTESIAN_POINT('Ctrl Pts',(-11.1812909210561,23.8640475726204,15.97983003041));
#10107=CARTESIAN_POINT('Ctrl Pts',(-10.0452414973032,24.2099754626599,15.69858003041));
#10108=CARTESIAN_POINT('Ctrl Pts',(-9.70013098088765,25.3460850661404,15.41733003041));
#10109=CARTESIAN_POINT('Ctrl Pts',(-10.4538244039853,26.2645547246601,15.13608003041));
#10110=CARTESIAN_POINT('Ctrl Pts',(-11.635843063436,26.14799088929,14.85483003041));
#10111=CARTESIAN_POINT('Ctrl Pts',(-12.1958123010896,25.1005009427962,14.57358003041));
#10112=CARTESIAN_POINT('Ctrl Pts',(-11.6358619781388,24.0529085194103,14.29233003041));
#10113=CARTESIAN_POINT('Ctrl Pts',(-10.4537769496115,23.9364993059084,14.01108003041));
#10114=CARTESIAN_POINT('Ctrl Pts',(-9.70023112780759,24.854683509662,13.72983003041));
#10115=CARTESIAN_POINT('Ctrl Pts',(-10.0450376142545,25.9913547946694,13.44858003041));
#10116=CARTESIAN_POINT('Ctrl Pts',(-11.1817035797842,26.3361568964569,13.16733003041));
#10117=CARTESIAN_POINT('Ctrl Pts',(-12.0998967445887,25.5826167555775,12.88608003041));
#10118=CARTESIAN_POINT('Ctrl Pts',(-11.9834703687346,24.4005218591871,12.60483003041));
#10119=CARTESIAN_POINT('Ctrl Pts',(-10.9359120418715,23.8405906121891,12.32358003041));
#10120=CARTESIAN_POINT('Ctrl Pts',(-9.88835371500838,24.4005218591871,12.04233003041));
#10121=CARTESIAN_POINT('Ctrl Pts',(-9.77192733915425,25.5826167555775,11.76108003041));
#10122=CARTESIAN_POINT('Ctrl Pts',(-10.6901205039588,26.3361568964569,11.47983003041));
#10123=CARTESIAN_POINT('Ctrl Pts',(-11.8267864694885,25.9913547946694,11.19858003041));
#10124=CARTESIAN_POINT('Ctrl Pts',(-12.1715929559354,24.854683509662,10.91733003041));
#10125=CARTESIAN_POINT('Ctrl Pts',(-11.4180471341314,23.9364993059084,10.63608003041));
#10126=CARTESIAN_POINT('Ctrl Pts',(-10.2359621056042,24.0529085194103,10.35483003041));
#10127=CARTESIAN_POINT('Ctrl Pts',(-9.6760117826534,25.1005009427962,10.07358003041));
#10128=CARTESIAN_POINT('Ctrl Pts',(-10.2359810203069,26.14799088929,9.79233003040999));
#10129=CARTESIAN_POINT('Ctrl Pts',(-11.4179996797577,26.2645547246602,9.51108003040999));
#10130=CARTESIAN_POINT('Ctrl Pts',(-12.1716931028553,25.3460850661404,9.22983003040999));
#10131=CARTESIAN_POINT('Ctrl Pts',(-11.8265825864398,24.2099754626599,8.94858003040999));
#10132=CARTESIAN_POINT('Ctrl Pts',(-10.6905331626869,23.8640475726204,8.66733003040999));
#10133=CARTESIAN_POINT('Ctrl Pts',(-9.77108168635966,24.6198771550135,8.38608003040999));
#10134=CARTESIAN_POINT('Ctrl Pts',(-9.8705209840808,25.6007219425128,8.15170503040999));
#10135=CARTESIAN_POINT('Ctrl Pts',(-10.4113171712369,26.0836714981141,7.96420503040999));
#10136=CARTESIAN_POINT('Ctrl Pts',(-10.7605277696664,26.1720429125025,7.87045503040999));
#10137=CARTESIAN_POINT('Ctrl Pts',(-10.9359120418715,26.1720429125025,7.82358003040999));
#10138=CARTESIAN_POINT('Ctrl Pts',(-10.9359120418715,26.1004782148047,16.6747998250855));
#10139=CARTESIAN_POINT('Ctrl Pts',(-11.0994166034008,26.1004782148047,16.6279248250855));
#10140=CARTESIAN_POINT('Ctrl Pts',(-11.4254947083535,26.0179576167138,16.5341748250855));
#10141=CARTESIAN_POINT('Ctrl Pts',(-11.9298938526699,25.5674231952741,16.3466748250855));
#10142=CARTESIAN_POINT('Ctrl Pts',(-12.022967290413,24.6519351730184,16.1122998250855));
#10143=CARTESIAN_POINT('Ctrl Pts',(-11.1648405798372,23.9467391142659,15.8310498250855));
#10144=CARTESIAN_POINT('Ctrl Pts',(-10.1048070365844,24.2694897541725,15.5497998250855));
#10145=CARTESIAN_POINT('Ctrl Pts',(-9.78273323261569,25.3296743778897,15.2685498250855));
#10146=CARTESIAN_POINT('Ctrl Pts',(-10.4860583036714,26.1867303933138,14.9872998250855));
#10147=CARTESIAN_POINT('Ctrl Pts',(-11.5890488871064,26.0779653129614,14.7060498250855));
#10148=CARTESIAN_POINT('Ctrl Pts',(-12.111587631401,25.100498383335,14.4247998250855));
#10149=CARTESIAN_POINT('Ctrl Pts',(-11.5890686614131,24.1229405170205,14.1435498250855));
#10150=CARTESIAN_POINT('Ctrl Pts',(-10.486008692659,24.0143126461238,13.8622998250855));
#10151=CARTESIAN_POINT('Ctrl Pts',(-9.7828379310398,24.8711153529452,13.5810498250855));
#10152=CARTESIAN_POINT('Ctrl Pts',(-10.1045938851323,25.9317984014709,13.2997998250855));
#10153=CARTESIAN_POINT('Ctrl Pts',(-11.1652720341777,26.2535501024307,13.0185498250855));
#10154=CARTESIAN_POINT('Ctrl Pts',(-12.0220827798711,25.5503851117544,12.7372998250855));
#10155=CARTESIAN_POINT('Ctrl Pts',(-11.9134396402228,24.4473149177691,12.4560498250855));
#10156=CARTESIAN_POINT('Ctrl Pts',(-10.9359120418715,23.9248158302944,12.1747998250855));
#10157=CARTESIAN_POINT('Ctrl Pts',(-9.95838444352014,24.4473149177691,11.8935498250855));
#10158=CARTESIAN_POINT('Ctrl Pts',(-9.84974130387186,25.5503851117544,11.6122998250855));
#10159=CARTESIAN_POINT('Ctrl Pts',(-10.7065520495652,26.2535501024307,11.3310498250855));
#10160=CARTESIAN_POINT('Ctrl Pts',(-11.7672301986107,25.9317984014709,11.0497998250855));
#10161=CARTESIAN_POINT('Ctrl Pts',(-12.0889861527032,24.8711153529452,10.7685498250855));
#10162=CARTESIAN_POINT('Ctrl Pts',(-11.385815391084,24.0143126461239,10.4872998250855));
#10163=CARTESIAN_POINT('Ctrl Pts',(-10.2827554223299,24.1229405170204,10.2060498250855));
#10164=CARTESIAN_POINT('Ctrl Pts',(-9.76023645234196,25.100498383335,9.92479982508547));
#10165=CARTESIAN_POINT('Ctrl Pts',(-10.2827751966365,26.0779653129613,9.64354982508548));
#10166=CARTESIAN_POINT('Ctrl Pts',(-11.3857657800716,26.1867303933138,9.36229982508546));
#10167=CARTESIAN_POINT('Ctrl Pts',(-12.0890908511273,25.3296743778897,9.08104982508548));
#10168=CARTESIAN_POINT('Ctrl Pts',(-11.7670170471586,24.2694897541725,8.79979982508546));
#10169=CARTESIAN_POINT('Ctrl Pts',(-10.7069835039058,23.9467391142658,8.51854982508547));
#10170=CARTESIAN_POINT('Ctrl Pts',(-9.84885679332996,24.6519351730184,8.23729982508548));
#10171=CARTESIAN_POINT('Ctrl Pts',(-9.94193023107313,25.5674231952741,8.00292482508547));
#10172=CARTESIAN_POINT('Ctrl Pts',(-10.4463293753895,26.0179576167137,7.81542482508547));
#10173=CARTESIAN_POINT('Ctrl Pts',(-10.7724074803422,26.1004782148047,7.72167482508547));
#10174=CARTESIAN_POINT('Ctrl Pts',(-10.9359120418715,26.1004782148047,7.67479982508547));
#10175=CARTESIAN_POINT('Ctrl Pts',(-10.9359120418715,26.1004782148047,16.6));
#10176=CARTESIAN_POINT('Ctrl Pts',(-11.099536659246,26.1004782148047,16.553125));
#10177=CARTESIAN_POINT('Ctrl Pts',(-11.425478146952,26.0179944258633,16.459375));
#10178=CARTESIAN_POINT('Ctrl Pts',(-11.9300789153048,25.5673438360005,16.271875));
#10179=CARTESIAN_POINT('Ctrl Pts',(-12.0229540626903,24.6519632977172,16.0375));
#10180=CARTESIAN_POINT('Ctrl Pts',(-11.164885722509,23.9466553694149,15.75625));
#10181=CARTESIAN_POINT('Ctrl Pts',(-10.1047480288197,24.2694595959893,15.475));
#10182=CARTESIAN_POINT('Ctrl Pts',(-9.7826825635668,25.329679981508,15.19375));
#10183=CARTESIAN_POINT('Ctrl Pts',(-10.4860312388173,26.1867889046978,14.9125));
#10184=CARTESIAN_POINT('Ctrl Pts',(-11.5890842776128,26.0780137287588,14.63125));
#10185=CARTESIAN_POINT('Ctrl Pts',(-12.1116466665383,25.1004991337717,14.35));
#10186=CARTESIAN_POINT('Ctrl Pts',(-11.5891025224479,24.1228902184961,14.06875));
#10187=CARTESIAN_POINT('Ctrl Pts',(-10.4859854650458,24.0142573573597,13.7875));
#10188=CARTESIAN_POINT('Ctrl Pts',(-9.78277916381912,24.8711035465199,13.50625));
#10189=CARTESIAN_POINT('Ctrl Pts',(-10.1045513655818,25.9318409055902,13.225));
#10190=CARTESIAN_POINT('Ctrl Pts',(-11.1652837785312,26.2536089704377,12.94375));
#10191=CARTESIAN_POINT('Ctrl Pts',(-12.0221382397948,25.5504081019422,12.6625));
#10192=CARTESIAN_POINT('Ctrl Pts',(-11.9134895714075,24.4472815516099,12.38125));
#10193=CARTESIAN_POINT('Ctrl Pts',(-10.9359120418715,23.9247557910194,12.1));
#10194=CARTESIAN_POINT('Ctrl Pts',(-9.95833451233548,24.4472815516099,11.81875));
#10195=CARTESIAN_POINT('Ctrl Pts',(-9.84968584394817,25.5504081019422,11.5375));
#10196=CARTESIAN_POINT('Ctrl Pts',(-10.7065403052118,26.2536089704376,11.25625));
#10197=CARTESIAN_POINT('Ctrl Pts',(-11.7672727181612,25.9318409055902,10.975));
#10198=CARTESIAN_POINT('Ctrl Pts',(-12.0890449199239,24.8711035465198,10.69375));
#10199=CARTESIAN_POINT('Ctrl Pts',(-11.3858386186972,24.0142573573597,10.4125));
#10200=CARTESIAN_POINT('Ctrl Pts',(-10.2827215612951,24.1228902184961,10.13125));
#10201=CARTESIAN_POINT('Ctrl Pts',(-9.76017741720471,25.1004991337717,9.85000000000001));
#10202=CARTESIAN_POINT('Ctrl Pts',(-10.2827398061301,26.0780137287587,9.56874999999999));
#10203=CARTESIAN_POINT('Ctrl Pts',(-11.3857928449257,26.1867889046978,9.28750000000001));
#10204=CARTESIAN_POINT('Ctrl Pts',(-12.0891415201762,25.329679981508,9.00624999999999));
#10205=CARTESIAN_POINT('Ctrl Pts',(-11.7670760549233,24.2694595959893,8.725));
#10206=CARTESIAN_POINT('Ctrl Pts',(-10.706938361234,23.946655369415,8.44375));
#10207=CARTESIAN_POINT('Ctrl Pts',(-9.84887002105266,24.6519632977172,8.1625));
#10208=CARTESIAN_POINT('Ctrl Pts',(-9.9417451684382,25.5673438360005,7.92812499999999));
#10209=CARTESIAN_POINT('Ctrl Pts',(-10.446345936791,26.0179944258633,7.740625));
#10210=CARTESIAN_POINT('Ctrl Pts',(-10.772287424497,26.1004782148047,7.646875));
#10211=CARTESIAN_POINT('Ctrl Pts',(-10.9359120418715,26.1004782148047,7.6));
#10212=CARTESIAN_POINT('',(-10.9359120418715,26.1004782148047,7.6));
#10213=CARTESIAN_POINT('Ctrl Pts',(-10.9359120418715,26.1004782148047,16.6));
#10214=CARTESIAN_POINT('Ctrl Pts',(-11.099536659246,26.1004782148047,16.553125));
#10215=CARTESIAN_POINT('Ctrl Pts',(-11.425478146952,26.0179944258633,16.459375));
#10216=CARTESIAN_POINT('Ctrl Pts',(-11.9300789153048,25.5673438360005,16.271875));
#10217=CARTESIAN_POINT('Ctrl Pts',(-12.0229540626903,24.6519632977172,16.0375));
#10218=CARTESIAN_POINT('Ctrl Pts',(-11.164885722509,23.9466553694149,15.75625));
#10219=CARTESIAN_POINT('Ctrl Pts',(-10.1047480288197,24.2694595959893,15.475));
#10220=CARTESIAN_POINT('Ctrl Pts',(-9.7826825635668,25.329679981508,15.19375));
#10221=CARTESIAN_POINT('Ctrl Pts',(-10.4860312388173,26.1867889046978,14.9125));
#10222=CARTESIAN_POINT('Ctrl Pts',(-11.5890842776128,26.0780137287588,14.63125));
#10223=CARTESIAN_POINT('Ctrl Pts',(-12.1116466665383,25.1004991337717,14.35));
#10224=CARTESIAN_POINT('Ctrl Pts',(-11.5891025224479,24.1228902184961,14.06875));
#10225=CARTESIAN_POINT('Ctrl Pts',(-10.4859854650458,24.0142573573597,13.7875));
#10226=CARTESIAN_POINT('Ctrl Pts',(-9.78277916381912,24.8711035465199,13.50625));
#10227=CARTESIAN_POINT('Ctrl Pts',(-10.1045513655818,25.9318409055902,13.225));
#10228=CARTESIAN_POINT('Ctrl Pts',(-11.1652837785312,26.2536089704377,12.94375));
#10229=CARTESIAN_POINT('Ctrl Pts',(-12.0221382397948,25.5504081019422,12.6625));
#10230=CARTESIAN_POINT('Ctrl Pts',(-11.9134895714075,24.4472815516099,12.38125));
#10231=CARTESIAN_POINT('Ctrl Pts',(-10.9359120418715,23.9247557910194,12.1));
#10232=CARTESIAN_POINT('Ctrl Pts',(-9.95833451233548,24.4472815516099,11.81875));
#10233=CARTESIAN_POINT('Ctrl Pts',(-9.84968584394817,25.5504081019422,11.5375));
#10234=CARTESIAN_POINT('Ctrl Pts',(-10.7065403052118,26.2536089704376,11.25625));
#10235=CARTESIAN_POINT('Ctrl Pts',(-11.7672727181612,25.9318409055902,10.975));
#10236=CARTESIAN_POINT('Ctrl Pts',(-12.0890449199239,24.8711035465198,10.69375));
#10237=CARTESIAN_POINT('Ctrl Pts',(-11.3858386186972,24.0142573573597,10.4125));
#10238=CARTESIAN_POINT('Ctrl Pts',(-10.2827215612951,24.1228902184961,10.13125));
#10239=CARTESIAN_POINT('Ctrl Pts',(-9.76017741720471,25.1004991337717,9.85000000000001));
#10240=CARTESIAN_POINT('Ctrl Pts',(-10.2827398061301,26.0780137287587,9.56874999999999));
#10241=CARTESIAN_POINT('Ctrl Pts',(-11.3857928449257,26.1867889046978,9.28750000000001));
#10242=CARTESIAN_POINT('Ctrl Pts',(-12.0891415201762,25.329679981508,9.00624999999999));
#10243=CARTESIAN_POINT('Ctrl Pts',(-11.7670760549233,24.2694595959893,8.725));
#10244=CARTESIAN_POINT('Ctrl Pts',(-10.706938361234,23.946655369415,8.44375));
#10245=CARTESIAN_POINT('Ctrl Pts',(-9.84887002105266,24.6519632977172,8.1625));
#10246=CARTESIAN_POINT('Ctrl Pts',(-9.9417451684382,25.5673438360005,7.92812499999999));
#10247=CARTESIAN_POINT('Ctrl Pts',(-10.446345936791,26.0179944258633,7.740625));
#10248=CARTESIAN_POINT('Ctrl Pts',(-10.772287424497,26.1004782148047,7.646875));
#10249=CARTESIAN_POINT('Ctrl Pts',(-10.9359120418715,26.1004782148047,7.6));
#10250=CARTESIAN_POINT('Origin',(-10.9359120418715,26.3504782148047,7.6));
#10251=CARTESIAN_POINT('Origin',(-10.9359120418715,26.3504782148047,7.6));
#11364=UNCERTAINTY_MEASURE_WITH_UNIT(LENGTH_MEASURE(0.01),#11386,
'DISTANCE_ACCURACY_VALUE',
'Maximum model space distance between geometric entities at asserted c
onnectivities');
#11370=UNCERTAINTY_MEASURE_WITH_UNIT(LENGTH_MEASURE(0.01),#11386,
'DISTANCE_ACCURACY_VALUE',
'Maximum model space distance between geometric entities at asserted c
onnectivities');
#11379=(
GEOMETRIC_REPRESENTATION_CONTEXT(3)
GLOBAL_UNCERTAINTY_ASSIGNED_CONTEXT((#11364))
GLOBAL_UNIT_ASSIGNED_CONTEXT((#11386,#11388,#11389))
REPRESENTATION_CONTEXT('','3D')
);
#11385=(
GEOMETRIC_REPRESENTATION_CONTEXT(3)
GLOBAL_UNCERTAINTY_ASSIGNED_CONTEXT((#11370))
GLOBAL_UNIT_ASSIGNED_CONTEXT((#11386,#11388,#11389))
REPRESENTATION_CONTEXT('','3D')
);
#11386=(
LENGTH_UNIT()
NAMED_UNIT(*)
SI_UNIT(.MILLI.,.METRE.)
);
#11388=(
NAMED_UNIT(*)
PLANE_ANGLE_UNIT()
SI_UNIT($,.RADIAN.)
);
#11389=(
NAMED_UNIT(*)
SI_UNIT($,.STERADIAN.)
SOLID_ANGLE_UNIT()
);
#11398=SHAPE_DEFINITION_REPRESENTATION(#11412,#11439);
#11412=PRODUCT_DEFINITION_SHAPE('',$,#11454);
#11439=SHAPE_REPRESENTATION('',(#6035),#11379);
#11445=PRODUCT_DEFINITION_CONTEXT('part definition',#11489,'design');
#11454=PRODUCT_DEFINITION('Spring_04','Spring_04',#11468,#11445);
#11468=PRODUCT_DEFINITION_FORMATION('',$,#11499);
#11489=APPLICATION_CONTEXT(
'Core Data for Automotive Mechanical Design Process');
#11490=PRODUCT_CONTEXT('part definition',#11489,'mechanical');
#11499=PRODUCT('Spring_04','Spring_04',$,(#11490));
#11561=COLOUR_RGB('Grey',0.48,0.52,0.57);
#11562=FILL_AREA_STYLE_COLOUR('',#11561);
#11563=FILL_AREA_STYLE('',(#11562));
#11564=SURFACE_STYLE_FILL_AREA(#11563);
#11565=SURFACE_SIDE_STYLE('',(#11564));
#11566=SURFACE_STYLE_USAGE(.BOTH.,#11565);
#11567=PRESENTATION_STYLE_ASSIGNMENT((#11566));
ENDSEC;
END-ISO-10303-21;
